ISO-10303-21;
HEADER;
FILE_DESCRIPTION (('STEP AP214'),
    '1' );
FILE_NAME ('slotted pan head screw_iso_ISO 1580 - M2 x 8 - 8N.step',
    '2026-10-27T14:18:53',
    ( '' ),
    ( '' ),
    'SwSTEP 2.0',
    'SolidWorks 2026',
    '' );
FILE_SCHEMA (( 'AUTOMOTIVE_DESIGN' ));
ENDSEC;

DATA;
#17=DIRECTION ( 'NONE',  ( 1.000000000000000000, -0.000000000000000000, -0.000000000000000000 ) ) ;
#26=EDGE_CURVE ( 'NONE', #2563, #1725, #4179, .T. ) ;
#35=FILL_AREA_STYLE ('',( #3774 ) ) ;
#67=ORIENTED_EDGE ( 'NONE', *, *, #3505, .F. ) ;
#74=CARTESIAN_POINT ( 'NONE',  ( -25.39999999999996305, 0.000000000000000000, 0.000000000000000000 ) ) ;
#86=( NAMED_UNIT ( * ) PLANE_ANGLE_UNIT ( ) SI_UNIT ( $, .RADIAN. ) );
#130=EDGE_CURVE ( 'NONE', #4142, #1478, #3633, .T. ) ;
#137=CARTESIAN_POINT ( 'NONE',  ( 0.5000000000000000000, 0.2499999999999982792, 2.000000000000001776 ) ) ;
#144=LINE ( 'NONE', #4359, #211 ) ;
#153=DIRECTION ( 'NONE',  ( 0.000000000000000000, 0.000000000000000000, 1.000000000000000000 ) ) ;
#158=ORIENTED_EDGE ( 'NONE', *, *, #2741, .F. ) ;
#160=CARTESIAN_POINT ( 'NONE',  ( 0.6000000000000000888, 0.000000000000000000, 0.000000000000000000 ) ) ;
#161=CARTESIAN_POINT ( 'NONE',  ( 0.5000000000000000000, 0.2499999999999982792, -2.000000000000000000 ) ) ;
#165=DIRECTION ( 'NONE',  ( 0.000000000000000000, 0.000000000000000000, 1.000000000000000000 ) ) ;
#210=TOROIDAL_SURFACE ( 'NONE', #5533, 1.336466033005844434, 0.5999999999999999778 ) ;
#211=VECTOR ( 'NONE', #2932, 1000.000000000000000 ) ;
#216=MANIFOLD_SOLID_BREP ( 'Slot', #3438 ) ;
#231=ORIENTED_EDGE ( 'NONE', *, *, #2067, .F. ) ;
#240=ORIENTED_EDGE ( 'NONE', *, *, #1900, .T. ) ;
#274=ORIENTED_EDGE ( 'NONE', *, *, #5318, .F. ) ;
#287=CARTESIAN_POINT ( 'NONE',  ( 0.5000000000000000000, 0.000000000000000000, 0.000000000000000000 ) ) ;
#295=CARTESIAN_POINT ( 'NONE',  ( 0.000000000000000000, -0.2499999999999999445, 1.312875263449798879 ) ) ;
#303=ORIENTED_EDGE ( 'NONE', *, *, #3462, .T. ) ;
#307=ORIENTED_EDGE ( 'NONE', *, *, #4245, .F. ) ;
#330=CARTESIAN_POINT ( 'NONE',  ( 8.300922883092140858E-17, -0.2499999999999997780, -1.455170506525537588 ) ) ;
#370=ORIENTED_EDGE ( 'NONE', *, *, #3462, .F. ) ;
#415=ORIENTED_EDGE ( 'NONE', *, *, #26, .F. ) ;
#421=CARTESIAN_POINT ( 'NONE',  ( 0.05011565059742434380, 0.2499999999999982792, -1.595010514166263382 ) ) ;
#429=ADVANCED_FACE ( 'NONE', ( #3884 ), #4687, .T. ) ;
#449=PLANE ( 'NONE',  #1541 ) ;
#450=CARTESIAN_POINT ( 'NONE',  ( 0.3600944671415647891, -0.2500000000000000000, 1.887947737020718941 ) ) ;
#479=VECTOR ( 'NONE', #645, 1000.000000000000000 ) ;
#486=AXIS2_PLACEMENT_3D ( 'NONE', #2448, #4210, #5240 ) ;
#488=DIRECTION ( 'NONE',  ( 1.000000000000000000, 0.000000000000000000, 0.000000000000000000 ) ) ;
#497=CARTESIAN_POINT ( 'NONE',  ( 0.000000000000000000, -0.2499999999999998335, -1.312875263449798879 ) ) ;
#509=ADVANCED_FACE ( 'NONE', ( #3345 ), #2461, .T. ) ;
#510=CARTESIAN_POINT ( 'NONE',  ( 0.6000000000000000888, 1.636698849489768475E-16, -1.336466033005844434 ) ) ;
#515=PRODUCT_CONTEXT ( 'NONE', #5629, 'mechanical' ) ;
#552=DIRECTION ( 'NONE',  ( -1.000000000000000000, -0.000000000000000000, -0.000000000000000000 ) ) ;
#557=DIRECTION ( 'NONE',  ( 0.000000000000000000, 0.000000000000000000, 1.000000000000000000 ) ) ;
#619=EDGE_LOOP ( 'NONE', ( #1180, #3918, #3535, #5634, #2377, #231, #3566, #1991 ) ) ;
#633=ORIENTED_EDGE ( 'NONE', *, *, #3059, .T. ) ;
#645=DIRECTION ( 'NONE',  ( 0.000000000000000000, 0.000000000000000000, -1.000000000000000000 ) ) ;
#658=CARTESIAN_POINT ( 'NONE',  ( 1.314929834301322591E-16, 0.000000000000000000, 0.000000000000000000 ) ) ;
#667=DIRECTION ( 'NONE',  ( 1.000000000000000000, 0.000000000000000000, 0.000000000000000000 ) ) ;
#668=CIRCLE ( 'NONE', #4059, 1.336466033005844434 ) ;
#671=CIRCLE ( 'NONE', #1146, 2.000000000000000000 ) ;
#696=VECTOR ( 'NONE', #1255, 1000.000000000000000 ) ;
#699=DIRECTION ( 'NONE',  ( 1.000000000000000000, 0.000000000000000000, 0.000000000000000000 ) ) ;
#708=VERTEX_POINT ( 'NONE', #3229 ) ;
#710=( NAMED_UNIT ( * ) PLANE_ANGLE_UNIT ( ) SI_UNIT ( $, .RADIAN. ) );
#717=EDGE_LOOP ( 'NONE', ( #3429, #5530, #303, #5193 ) ) ;
#724=DIRECTION ( 'NONE',  ( 0.000000000000000000, 1.065814103640150121E-14, 1.000000000000000000 ) ) ;
#755=EDGE_CURVE ( 'NONE', #2883, #5520, #1571, .T. ) ;
#757=CARTESIAN_POINT ( 'NONE',  ( 1.299999999999999156, 0.000000000000000000, 0.000000000000000000 ) ) ;
#772=CARTESIAN_POINT ( 'NONE',  ( 0.5000000000000000000, -0.2499999999999997780, -1.911797424705720116 ) ) ;
#781=CARTESIAN_POINT ( 'NONE',  ( 0.5000000000000000000, 0.000000000000000000, 1.928074011315806136 ) ) ;
#786=EDGE_LOOP ( 'NONE', ( #1518, #4648, #5760, #5056 ) ) ;
#789=AXIS2_PLACEMENT_3D ( 'NONE', #658, #2109, #3959 ) ;
#806=CARTESIAN_POINT ( 'NONE',  ( 0.3612935698783896754, -0.2499999999999997224, -1.888152147991466245 ) ) ;
#838=DIRECTION ( 'NONE',  ( -1.000000000000000000, -0.000000000000000000, -0.000000000000000000 ) ) ;
#841=CARTESIAN_POINT ( 'NONE',  ( 0.2307700686259116507, -0.2500000000000000000, 1.812750528907549175 ) ) ;
#844=EDGE_LOOP ( 'NONE', ( #1420, #2357 ) ) ;
#845=ADVANCED_FACE ( 'NONE', ( #4282 ), #4736, .F. ) ;
#846=( NAMED_UNIT ( * ) PLANE_ANGLE_UNIT ( ) SI_UNIT ( $, .RADIAN. ) );
#862=ORIENTED_EDGE ( 'NONE', *, *, #5334, .T. ) ;
#883=AXIS2_PLACEMENT_3D ( 'NONE', #287, #2709, #1286 ) ;
#890=DIRECTION ( 'NONE',  ( 0.000000000000000000, 0.000000000000000000, 1.000000000000000000 ) ) ;
#897=CARTESIAN_POINT ( 'NONE',  ( 0.000000000000000000, 0.2499999999999982792, -1.312875263449799323 ) ) ;
#901=CARTESIAN_POINT ( 'NONE',  ( 0.000000000000000000, 0.2499999999999982792, 1.312875263449799323 ) ) ;
#911=CARTESIAN_POINT ( 'NONE',  ( 0.5000000000000000000, -0.2499999999999997780, -1.911797424705720116 ) ) ;
#918=ORIENTED_EDGE ( 'NONE', *, *, #3750, .T. ) ;
#972=DIRECTION ( 'NONE',  ( 0.000000000000000000, 0.000000000000000000, 1.000000000000000000 ) ) ;
#992=CIRCLE ( 'NONE', #5547, 1.000000000000000000 ) ;
#993=SURFACE_SIDE_STYLE ('',( #4244 ) ) ;
#997=CARTESIAN_POINT ( 'NONE',  ( -5.404070203482436163E-16, 0.2499999999999982792, 1.454823465665887605 ) ) ;
#1013=DIRECTION ( 'NONE',  ( -1.000000000000000000, -0.000000000000000000, -0.000000000000000000 ) ) ;
#1031=LINE ( 'NONE', #137, #479 ) ;
#1036=CARTESIAN_POINT ( 'NONE',  ( 1.084202172485504434E-16, 0.000000000000000000, 0.000000000000000000 ) ) ;
#1065=CARTESIAN_POINT ( 'NONE',  ( 0.5000000000000000000, 2.361209666477099964E-16, -1.928074011315806136 ) ) ;
#1095=CARTESIAN_POINT ( 'NONE',  ( 1.299999999999999156, 0.000000000000000000, 0.000000000000000000 ) ) ;
#1119=ADVANCED_FACE ( 'NONE', ( #1670 ), #4896, .T. ) ;
#1146=AXIS2_PLACEMENT_3D ( 'NONE', #2308, #3712, #890 ) ;
#1150=B_SPLINE_CURVE_WITH_KNOTS ( 'NONE', 3,
 ( #5395, #4613, #3157, #841, #450, #4579 ),
 .UNSPECIFIED., .F., .F.,
 ( 4, 2, 4 ),
 ( 0.0005861251363949650413, 0.001008091297609326094, 0.001430057458823687363 ),
 .UNSPECIFIED. ) ;
#1152=( NAMED_UNIT ( * ) SI_UNIT ( $, .STERADIAN. ) SOLID_ANGLE_UNIT ( ) );
#1164=CARTESIAN_POINT ( 'NONE',  ( 0.6000000000000000888, 0.000000000000000000, 1.336466033005844434 ) ) ;
#1180=ORIENTED_EDGE ( 'NONE', *, *, #1410, .F. ) ;
#1226=AXIS2_PLACEMENT_3D ( 'NONE', #1164, #3513, #2081 ) ;
#1239=DIRECTION ( 'NONE',  ( 0.000000000000000000, 0.000000000000000000, -1.000000000000000000 ) ) ;
#1255=DIRECTION ( 'NONE',  ( 0.000000000000000000, 0.000000000000000000, -1.000000000000000000 ) ) ;
#1286=DIRECTION ( 'NONE',  ( 0.000000000000000000, 0.000000000000000000, 1.000000000000000000 ) ) ;
#1299=FACE_OUTER_BOUND ( 'NONE', #2214, .T. ) ;
#1383=EDGE_CURVE ( 'NONE', #1757, #3457, #5628, .T. ) ;
#1386=STYLED_ITEM ( 'NONE', ( #4673 ), #5436 ) ;
#1410=EDGE_CURVE ( 'NONE', #5520, #2063, #5108, .T. ) ;
#1417=DIRECTION ( 'NONE',  ( -1.000000000000000000, -0.000000000000000000, -0.000000000000000000 ) ) ;
#1420=ORIENTED_EDGE ( 'NONE', *, *, #4411, .F. ) ;
#1442=CARTESIAN_POINT ( 'NONE',  ( 0.2309188673393134938, 0.2499999999999982792, 1.812888087824517713 ) ) ;
#1475=CARTESIAN_POINT ( 'NONE',  ( -25.39999999999996305, 0.000000000000000000, 1.000000000000000000 ) ) ;
#1478=VERTEX_POINT ( 'NONE', #295 ) ;
#1504=SURFACE_STYLE_USAGE ( .BOTH. , #993 ) ;
#1511=AXIS2_PLACEMENT_3D ( 'NONE', #510, #2360, #5596 ) ;
#1518=ORIENTED_EDGE ( 'NONE', *, *, #5400, .T. ) ;
#1526=EDGE_CURVE ( 'NONE', #2883, #4824, #2387, .T. ) ;
#1529=ORIENTED_EDGE ( 'NONE', *, *, #4214, .F. ) ;
#1535=CARTESIAN_POINT ( 'NONE',  ( 0.5000000000000000000, 0.2499999999999982792, -1.911797424705720339 ) ) ;
#1541=AXIS2_PLACEMENT_3D ( 'NONE', #2073, #2521, #5804 ) ;
#1543=ADVANCED_FACE ( 'NONE', ( #3929 ), #2565, .T. ) ;
#1571=CIRCLE ( 'NONE', #3608, 1.934182851860892116 ) ;
#1611=AXIS2_PLACEMENT_3D ( 'NONE', #74, #3401, #2430 ) ;
#1631=CARTESIAN_POINT ( 'NONE',  ( 0.5477065543514070267, 2.408992218395923449E-16, 1.934182851860892116 ) ) ;
#1635=PRODUCT ( 'slotted pan head screw_iso_ISO 1580 - M2 x 8 - 8N', 'slotted pan head screw_iso_ISO 1580 - M2 x 8 - 8N', '', ( #515 ) ) ;
#1670=FACE_OUTER_BOUND ( 'NONE', #1860, .T. ) ;
#1671=AXIS2_PLACEMENT_3D ( 'NONE', #160, #4228, #5194 ) ;
#1678=COLOUR_RGB ( '',1.000000000000000000, 0.9490196078431372140, 0.9098039215686274384 ) ;
#1693=PRODUCT_DEFINITION_CONTEXT ( 'detailed design', #2734, 'design' ) ;
#1712=CARTESIAN_POINT ( 'NONE',  ( 0.04978537780227577231, -0.2499999999999997224, -1.594765474869573874 ) ) ;
#1725=VERTEX_POINT ( 'NONE', #4049 ) ;
#1738=LINE ( 'NONE', #2102, #4679 ) ;
#1757=VERTEX_POINT ( 'NONE', #3120 ) ;
#1774=CARTESIAN_POINT ( 'NONE',  ( 0.000000000000000000, 0.000000000000000000, -1.886264737416298409 ) ) ;
#1779=( GEOMETRIC_REPRESENTATION_CONTEXT ( 3 ) GLOBAL_UNCERTAINTY_ASSIGNED_CONTEXT ( ( #2595 ) ) GLOBAL_UNIT_ASSIGNED_CONTEXT ( ( #3361, #86, #3696 ) ) REPRESENTATION_CONTEXT ( 'NONE', 'WORKASPACE' ) );
#1790=EDGE_CURVE ( 'NONE', #3934, #1757, #2416, .T. ) ;
#1826=B_SPLINE_CURVE_WITH_KNOTS ( 'NONE', 3,
 ( #4276, #2363, #1442, #3304, #997, #1901 ),
 .UNSPECIFIED., .F., .F.,
 ( 4, 2, 4 ),
 ( 0.002363858439908544419, 0.002786031303543298580, 0.003208204167178053175 ),
 .UNSPECIFIED. ) ;
#1851=ORIENTED_EDGE ( 'NONE', *, *, #2278, .F. ) ;
#1860=EDGE_LOOP ( 'NONE', ( #2516, #2216, #3733, #370 ) ) ;
#1888=CARTESIAN_POINT ( 'NONE',  ( 0.000000000000000000, -0.2499999999999997780, -2.000000000000000000 ) ) ;
#1900=EDGE_CURVE ( 'NONE', #1962, #708, #668, .T. ) ;
#1901=CARTESIAN_POINT ( 'NONE',  ( 0.000000000000000000, 0.2499999999999982792, 1.312875263449799323 ) ) ;
#1910=DIRECTION ( 'NONE',  ( 0.000000000000000000, 0.000000000000000000, 1.000000000000000000 ) ) ;
#1919=AXIS2_PLACEMENT_3D ( 'NONE', #1036, #2038, #5226 ) ;
#1962=VERTEX_POINT ( 'NONE', #901 ) ;
#1968=ADVANCED_FACE ( 'NONE', ( #2756, #4612 ), #449, .F. ) ;
#1989=CARTESIAN_POINT ( 'NONE',  ( 0.3608130681495591019, 0.2499999999999982792, -1.888070236890895703 ) ) ;
#1991=ORIENTED_EDGE ( 'NONE', *, *, #5517, .T. ) ;
#1997=DIRECTION ( 'NONE',  ( -1.000000000000000000, 0.000000000000000000, 0.000000000000000000 ) ) ;
#2038=DIRECTION ( 'NONE',  ( -1.000000000000000000, -0.000000000000000000, -0.000000000000000000 ) ) ;
#2061=CARTESIAN_POINT ( 'NONE',  ( 0.000000000000000000, 0.000000000000000000, 0.000000000000000000 ) ) ;
#2063=VERTEX_POINT ( 'NONE', #1065 ) ;
#2067=EDGE_CURVE ( 'NONE', #4142, #1478, #4837, .T. ) ;
#2073=CARTESIAN_POINT ( 'NONE',  ( 1.299999999999999600, 1.000000000000000000, 0.000000000000000000 ) ) ;
#2081=DIRECTION ( 'NONE',  ( 0.000000000000000000, 0.000000000000000000, -1.000000000000000000 ) ) ;
#2102=CARTESIAN_POINT ( 'NONE',  ( -25.39999999999996305, 1.224646799147353207E-16, -1.000000000000000000 ) ) ;
#2105=EDGE_LOOP ( 'NONE', ( #918, #67, #158, #3993, #3382, #4734 ) ) ;
#2109=DIRECTION ( 'NONE',  ( -1.000000000000000000, 0.000000000000000000, -0.000000000000000000 ) ) ;
#2132=CARTESIAN_POINT ( 'NONE',  ( 9.300000000000002487, 1.224646799147353207E-16, -1.000000000000000000 ) ) ;
#2136=ORIENTED_EDGE ( 'NONE', *, *, #1383, .F. ) ;
#2137=CARTESIAN_POINT ( 'NONE',  ( -25.39999999999996305, 0.000000000000000000, 0.000000000000000000 ) ) ;
#2150=AXIS2_PLACEMENT_3D ( 'NONE', #1095, #552, #165 ) ;
#2170=EDGE_LOOP ( 'NONE', ( #4031, #5677, #4572, #2136 ) ) ;
#2177=LINE ( 'NONE', #5042, #4969 ) ;
#2214=EDGE_LOOP ( 'NONE', ( #862, #5421, #633, #4556 ) ) ;
#2216=ORIENTED_EDGE ( 'NONE', *, *, #5552, .T. ) ;
#2230=MECHANICAL_DESIGN_GEOMETRIC_PRESENTATION_REPRESENTATION('',(#4660),#4072);
#2248=AXIS2_PLACEMENT_3D ( 'NONE', #3722, #3270, #5123 ) ;
#2254=EDGE_CURVE ( 'NONE', #2063, #5408, #4362, .T. ) ;
#2263=CARTESIAN_POINT ( 'NONE',  ( 0.2300425840023382074, 0.2499999999999982236, -1.812072026511089229 ) ) ;
#2278=EDGE_CURVE ( 'NONE', #1725, #2563, #671, .T. ) ;
#2304=VERTEX_POINT ( 'NONE', #5502 ) ;
#2308=CARTESIAN_POINT ( 'NONE',  ( 1.299999999999999156, 0.000000000000000000, 0.000000000000000000 ) ) ;
#2319=CARTESIAN_POINT ( 'NONE',  ( 0.5000000000000000000, 0.2499999999999982792, 1.911797424705720339 ) ) ;
#2357=ORIENTED_EDGE ( 'NONE', *, *, #1790, .F. ) ;
#2360=DIRECTION ( 'NONE',  ( -0.000000000000000000, 1.000000000000000000, 1.224646799147353207E-16 ) ) ;
#2363=CARTESIAN_POINT ( 'NONE',  ( 0.3609765494018736809, 0.2499999999999982792, 1.888098105530059190 ) ) ;
#2377=ORIENTED_EDGE ( 'NONE', *, *, #3059, .F. ) ;
#2384=EDGE_CURVE ( 'NONE', #3113, #5408, #1031, .T. ) ;
#2387=CIRCLE ( 'NONE', #1226, 0.5999999999999999778 ) ;
#2389=DIRECTION ( 'NONE',  ( 0.000000000000000000, 0.000000000000000000, 1.000000000000000000 ) ) ;
#2416=CIRCLE ( 'NONE', #4163, 1.000000000000000000 ) ;
#2422=EDGE_LOOP ( 'NONE', ( #307, #3684, #3948, #4372, #5003, #2849, #2923, #2505 ) ) ;
#2430=DIRECTION ( 'NONE',  ( 0.000000000000000000, 0.000000000000000000, 1.000000000000000000 ) ) ;
#2448=CARTESIAN_POINT ( 'NONE',  ( 0.5000000000000000000, 0.000000000000000000, 0.000000000000000000 ) ) ;
#2461=PLANE ( 'NONE',  #3456 ) ;
#2505=ORIENTED_EDGE ( 'NONE', *, *, #1526, .F. ) ;
#2516=ORIENTED_EDGE ( 'NONE', *, *, #4245, .T. ) ;
#2521=DIRECTION ( 'NONE',  ( -1.000000000000000000, 0.000000000000000000, -0.000000000000000000 ) ) ;
#2553=ORIENTED_EDGE ( 'NONE', *, *, #4220, .T. ) ;
#2559=ORIENTED_EDGE ( 'NONE', *, *, #2067, .T. ) ;
#2563=VERTEX_POINT ( 'NONE', #2609 ) ;
#2565=CYLINDRICAL_SURFACE ( 'NONE', #5680, 1.000000000000000000 ) ;
#2569=CARTESIAN_POINT ( 'NONE',  ( 0.5477065543514070267, 0.000000000000000000, -1.934182851860892116 ) ) ;
#2583=EDGE_LOOP ( 'NONE', ( #415, #1851 ) ) ;
#2586=CARTESIAN_POINT ( 'NONE',  ( 9.299999999999998934, 1.000000000000000000, 0.000000000000000000 ) ) ;
#2595=UNCERTAINTY_MEASURE_WITH_UNIT (LENGTH_MEASURE( 1.000000000000000082E-05 ), #3361, 'distance_accuracy_value', 'NONE');
#2609=CARTESIAN_POINT ( 'NONE',  ( 1.299999999999999156, 0.000000000000000000, -2.000000000000000000 ) ) ;
#2621=CARTESIAN_POINT ( 'NONE',  ( 0.2309054577385447060, -0.2499999999999997780, -1.812959136724909159 ) ) ;
#2628=VECTOR ( 'NONE', #2656, 1000.000000000000000 ) ;
#2656=DIRECTION ( 'NONE',  ( 0.9961946980917455452, 0.000000000000000000, -0.08715574274765848506 ) ) ;
#2671=DIRECTION ( 'NONE',  ( 0.000000000000000000, 0.000000000000000000, 1.000000000000000000 ) ) ;
#2686=DIRECTION ( 'NONE',  ( 0.000000000000000000, 0.000000000000000000, 1.000000000000000000 ) ) ;
#2688=DIRECTION ( 'NONE',  ( 0.000000000000000000, 0.000000000000000000, 1.000000000000000000 ) ) ;
#2692=PLANE ( 'NONE',  #3320 ) ;
#2695=( LENGTH_UNIT ( ) NAMED_UNIT ( * ) SI_UNIT ( .MILLI., .METRE. ) );
#2709=DIRECTION ( 'NONE',  ( 1.000000000000000000, -0.000000000000000000, -0.000000000000000000 ) ) ;
#2711=ORIENTED_EDGE ( 'NONE', *, *, #1790, .T. ) ;
#2722=PLANE ( 'NONE',  #2248 ) ;
#2723=DIRECTION ( 'NONE',  ( 0.000000000000000000, -1.000000000000000000, -5.421010862427519705E-17 ) ) ;
#2727=SHAPE_DEFINITION_REPRESENTATION ( #4552, #5016 ) ;
#2734=APPLICATION_CONTEXT ( 'automotive_design' ) ;
#2739=AXIS2_PLACEMENT_3D ( 'NONE', #5700, #488, #3371 ) ;
#2741=EDGE_CURVE ( 'NONE', #3113, #4824, #3106, .T. ) ;
#2753=CARTESIAN_POINT ( 'NONE',  ( -1.470152734901925752E-14, 0.2499999999999982792, -1.453737367178236983 ) ) ;
#2756=FACE_OUTER_BOUND ( 'NONE', #2583, .T. ) ;
#2805=AXIS2_PLACEMENT_3D ( 'NONE', #3677, #17, #972 ) ;
#2814=DIRECTION ( 'NONE',  ( -1.000000000000000000, -0.000000000000000000, -0.000000000000000000 ) ) ;
#2823=CIRCLE ( 'NONE', #883, 1.928074011315806136 ) ;
#2837=CARTESIAN_POINT ( 'NONE',  ( 1.084202172485504434E-16, 0.000000000000000000, 0.000000000000000000 ) ) ;
#2849=ORIENTED_EDGE ( 'NONE', *, *, #4434, .F. ) ;
#2883=VERTEX_POINT ( 'NONE', #1631 ) ;
#2923=ORIENTED_EDGE ( 'NONE', *, *, #2741, .T. ) ;
#2928=AXIS2_PLACEMENT_3D ( 'NONE', #5616, #3041, #4718 ) ;
#2932=DIRECTION ( 'NONE',  ( 0.000000000000000000, -5.421010862427519705E-17, 1.000000000000000000 ) ) ;
#2971=FACE_OUTER_BOUND ( 'NONE', #2422, .T. ) ;
#3027=CIRCLE ( 'NONE', #2150, 1.000000000000000000 ) ;
#3031=DIRECTION ( 'NONE',  ( 1.000000000000000000, -0.000000000000000000, -0.000000000000000000 ) ) ;
#3041=DIRECTION ( 'NONE',  ( 1.000000000000000000, 0.000000000000000000, 0.000000000000000000 ) ) ;
#3059=EDGE_CURVE ( 'NONE', #1478, #2304, #1150, .T. ) ;
#3106=CIRCLE ( 'NONE', #486, 1.928074011315806136 ) ;
#3113=VERTEX_POINT ( 'NONE', #2319 ) ;
#3120=CARTESIAN_POINT ( 'NONE',  ( 9.300000000000002487, 0.000000000000000000, 1.000000000000000000 ) ) ;
#3157=CARTESIAN_POINT ( 'NONE',  ( 0.05007909176323187272, -0.2500000000000000000, 1.595164775286565861 ) ) ;
#3176=EDGE_LOOP ( 'NONE', ( #2553, #4671 ) ) ;
#3229=CARTESIAN_POINT ( 'NONE',  ( 0.000000000000000000, 0.2499999999999982792, -1.312875263449799323 ) ) ;
#3270=DIRECTION ( 'NONE',  ( -1.000000000000000000, 0.000000000000000000, -0.000000000000000000 ) ) ;
#3304=CARTESIAN_POINT ( 'NONE',  ( 0.05007509226404533581, 0.2499999999999982236, 1.595201548406556480 ) ) ;
#3320=AXIS2_PLACEMENT_3D ( 'NONE', #3637, #2723, #4582 ) ;
#3345=FACE_OUTER_BOUND ( 'NONE', #2105, .T. ) ;
#3349=ADVANCED_FACE ( 'NONE', ( #4421 ), #5300, .T. ) ;
#3361=( LENGTH_UNIT ( ) NAMED_UNIT ( * ) SI_UNIT ( .MILLI., .METRE. ) );
#3371=DIRECTION ( 'NONE',  ( 0.000000000000000000, 0.000000000000000000, -1.000000000000000000 ) ) ;
#3382=ORIENTED_EDGE ( 'NONE', *, *, #2254, .F. ) ;
#3401=DIRECTION ( 'NONE',  ( -1.000000000000000000, -0.000000000000000000, -0.000000000000000000 ) ) ;
#3405=DIRECTION ( 'NONE',  ( -1.000000000000000000, -0.000000000000000000, -0.000000000000000000 ) ) ;
#3426=ORIENTED_EDGE ( 'NONE', *, *, #130, .F. ) ;
#3429=ORIENTED_EDGE ( 'NONE', *, *, #5552, .F. ) ;
#3433=UNCERTAINTY_MEASURE_WITH_UNIT (LENGTH_MEASURE( 1.000000000000000082E-05 ), #3920, 'distance_accuracy_value', 'NONE');
#3438=CLOSED_SHELL ( 'NONE', ( #4588, #1119, #1543, #3618, #429, #3349, #5794, #5866, #1968, #5839, #845, #4801, #509 ) ) ;
#3456=AXIS2_PLACEMENT_3D ( 'NONE', #161, #1997, #3849 ) ;
#3457=VERTEX_POINT ( 'NONE', #3591 ) ;
#3462=EDGE_CURVE ( 'NONE', #5520, #2563, #5476, .T. ) ;
#3505=EDGE_CURVE ( 'NONE', #4824, #2304, #2823, .T. ) ;
#3513=DIRECTION ( 'NONE',  ( 0.000000000000000000, -1.000000000000000000, 0.000000000000000000 ) ) ;
#3527=CARTESIAN_POINT ( 'NONE',  ( 0.000000000000000000, 0.000000000000000000, 0.000000000000000000 ) ) ;
#3535=ORIENTED_EDGE ( 'NONE', *, *, #1526, .T. ) ;
#3545=CARTESIAN_POINT ( 'NONE',  ( 9.300000000000002487, 0.000000000000000000, 0.000000000000000000 ) ) ;
#3566=ORIENTED_EDGE ( 'NONE', *, *, #5334, .F. ) ;
#3591=CARTESIAN_POINT ( 'NONE',  ( 1.299999999999999156, 0.000000000000000000, 1.000000000000000000 ) ) ;
#3608=AXIS2_PLACEMENT_3D ( 'NONE', #3643, #4994, #2671 ) ;
#3618=ADVANCED_FACE ( 'NONE', ( #5691 ), #4791, .T. ) ;
#3624=AXIS2_PLACEMENT_3D ( 'NONE', #2061, #699, #1239 ) ;
#3633=LINE ( 'NONE', #1888, #5905 ) ;
#3637=CARTESIAN_POINT ( 'NONE',  ( 0.5000000000000000000, -0.2499999999999997780, -2.000000000000000000 ) ) ;
#3643=CARTESIAN_POINT ( 'NONE',  ( 0.5477065543514070267, 0.000000000000000000, 0.000000000000000000 ) ) ;
#3677=CARTESIAN_POINT ( 'NONE',  ( 0.5000000000000000000, 0.000000000000000000, 0.000000000000000000 ) ) ;
#3684=ORIENTED_EDGE ( 'NONE', *, *, #1410, .T. ) ;
#3696=( NAMED_UNIT ( * ) SI_UNIT ( $, .STERADIAN. ) SOLID_ANGLE_UNIT ( ) );
#3708=VERTEX_POINT ( 'NONE', #4427 ) ;
#3712=DIRECTION ( 'NONE',  ( -1.000000000000000000, -0.000000000000000000, -0.000000000000000000 ) ) ;
#3722=CARTESIAN_POINT ( 'NONE',  ( 1.314929834301322591E-16, 0.000000000000000000, 0.000000000000000000 ) ) ;
#3731=CARTESIAN_POINT ( 'NONE',  ( 0.5000000000000000000, 0.2499999999999982792, 2.000000000000001776 ) ) ;
#3733=ORIENTED_EDGE ( 'NONE', *, *, #2278, .T. ) ;
#3750=EDGE_CURVE ( 'NONE', #4296, #2304, #144, .T. ) ;
#3773=B_SPLINE_CURVE_WITH_KNOTS ( 'NONE', 3,
 ( #772, #806, #2621, #1712, #330, #5414 ),
 .UNSPECIFIED., .F., .F.,
 ( 4, 2, 4 ),
 ( 0.003549988921687060456, 0.003971677118101641160, 0.004393365314516220997 ),
 .UNSPECIFIED. ) ;
#3774=FILL_AREA_STYLE_COLOUR ( '', #1678 ) ;
#3849=DIRECTION ( 'NONE',  ( 0.000000000000000000, 0.000000000000000000, 1.000000000000000000 ) ) ;
#3884=FACE_OUTER_BOUND ( 'NONE', #4962, .T. ) ;
#3908=CARTESIAN_POINT ( 'NONE',  ( 0.6000000000000000888, 0.000000000000000000, 0.000000000000000000 ) ) ;
#3918=ORIENTED_EDGE ( 'NONE', *, *, #755, .F. ) ;
#3920=( LENGTH_UNIT ( ) NAMED_UNIT ( * ) SI_UNIT ( .MILLI., .METRE. ) );
#3929=FACE_OUTER_BOUND ( 'NONE', #2170, .T. ) ;
#3934=VERTEX_POINT ( 'NONE', #2132 ) ;
#3948=ORIENTED_EDGE ( 'NONE', *, *, #2254, .T. ) ;
#3959=DIRECTION ( 'NONE',  ( -0.000000000000000000, 0.000000000000000000, 1.000000000000000000 ) ) ;
#3978=EDGE_CURVE ( 'NONE', #3934, #3708, #1738, .T. ) ;
#3993=ORIENTED_EDGE ( 'NONE', *, *, #2384, .T. ) ;
#4004=B_SPLINE_CURVE_WITH_KNOTS ( 'NONE', 3,
 ( #897, #2753, #421, #2263, #1989, #1535 ),
 .UNSPECIFIED., .F., .F.,
 ( 4, 2, 4 ),
 ( 0.003191392849877886309, 0.003612977948258624256, 0.004034563046639362202 ),
 .UNSPECIFIED. ) ;
#4031=ORIENTED_EDGE ( 'NONE', *, *, #4411, .T. ) ;
#4049=CARTESIAN_POINT ( 'NONE',  ( 1.299999999999999156, 2.449293598294706414E-16, 2.000000000000000000 ) ) ;
#4059=AXIS2_PLACEMENT_3D ( 'NONE', #2837, #1013, #557 ) ;
#4072=( GEOMETRIC_REPRESENTATION_CONTEXT ( 3 ) GLOBAL_UNCERTAINTY_ASSIGNED_CONTEXT ( ( #3433 ) ) GLOBAL_UNIT_ASSIGNED_CONTEXT ( ( #3920, #710, #1152 ) ) REPRESENTATION_CONTEXT ( 'NONE', 'WORKASPACE' ) );
#4080=LINE ( 'NONE', #5808, #696 ) ;
#4135=VECTOR ( 'NONE', #2814, 1000.000000000000000 ) ;
#4142=VERTEX_POINT ( 'NONE', #497 ) ;
#4147=DIRECTION ( 'NONE',  ( 0.000000000000000000, -5.421010862427519705E-17, 1.000000000000000000 ) ) ;
#4163=AXIS2_PLACEMENT_3D ( 'NONE', #3545, #5039, #2688 ) ;
#4167=AXIS2_PLACEMENT_3D ( 'NONE', #5009, #838, #2686 ) ;
#4179=CIRCLE ( 'NONE', #4167, 2.000000000000000000 ) ;
#4187=SHAPE_REPRESENTATION_RELATIONSHIP ( 'NONE' , 'NONE' ,  #5016, #5436 ) ;
#4190=CIRCLE ( 'NONE', #4287, 1.928074011315806136 ) ;
#4210=DIRECTION ( 'NONE',  ( 1.000000000000000000, -0.000000000000000000, -0.000000000000000000 ) ) ;
#4214=EDGE_CURVE ( 'NONE', #3708, #3457, #992, .T. ) ;
#4220=EDGE_CURVE ( 'NONE', #3457, #3708, #3027, .T. ) ;
#4224=DIRECTION ( 'NONE',  ( 0.000000000000000000, 1.000000000000000000, 0.000000000000000000 ) ) ;
#4228=DIRECTION ( 'NONE',  ( -1.000000000000000000, -0.000000000000000000, -0.000000000000000000 ) ) ;
#4244=SURFACE_STYLE_FILL_AREA ( #35 ) ;
#4245=EDGE_CURVE ( 'NONE', #5520, #2883, #4388, .T. ) ;
#4276=CARTESIAN_POINT ( 'NONE',  ( 0.5000000000000000000, 0.2499999999999982792, 1.911797424705720339 ) ) ;
#4282=FACE_OUTER_BOUND ( 'NONE', #786, .T. ) ;
#4287=AXIS2_PLACEMENT_3D ( 'NONE', #5339, #3031, #724 ) ;
#4296=VERTEX_POINT ( 'NONE', #911 ) ;
#4316=FACE_OUTER_BOUND ( 'NONE', #619, .T. ) ;
#4324=ORIENTED_EDGE ( 'NONE', *, *, #3978, .F. ) ;
#4359=CARTESIAN_POINT ( 'NONE',  ( 0.5000000000000000000, -0.2499999999999997780, -2.000000000000000000 ) ) ;
#4362=CIRCLE ( 'NONE', #2805, 1.928074011315806136 ) ;
#4372=ORIENTED_EDGE ( 'NONE', *, *, #5400, .F. ) ;
#4388=CIRCLE ( 'NONE', #2928, 1.934182851860892116 ) ;
#4395=( GEOMETRIC_REPRESENTATION_CONTEXT ( 3 ) GLOBAL_UNCERTAINTY_ASSIGNED_CONTEXT ( ( #5873 ) ) GLOBAL_UNIT_ASSIGNED_CONTEXT ( ( #2695, #846, #5942 ) ) REPRESENTATION_CONTEXT ( 'NONE', 'WORKASPACE' ) );
#4411=EDGE_CURVE ( 'NONE', #1757, #3934, #4490, .T. ) ;
#4421=FACE_OUTER_BOUND ( 'NONE', #844, .T. ) ;
#4424=ORIENTED_EDGE ( 'NONE', *, *, #1383, .T. ) ;
#4426=DIRECTION ( 'NONE',  ( -1.000000000000000000, -0.000000000000000000, -0.000000000000000000 ) ) ;
#4427=CARTESIAN_POINT ( 'NONE',  ( 1.299999999999999156, 1.224646799147353207E-16, -1.000000000000000000 ) ) ;
#4434=EDGE_CURVE ( 'NONE', #3113, #1962, #1826, .T. ) ;
#4490=CIRCLE ( 'NONE', #4585, 1.000000000000000000 ) ;
#4515=DIRECTION ( 'NONE',  ( -1.000000000000000000, -0.000000000000000000, -0.000000000000000000 ) ) ;
#4552=PRODUCT_DEFINITION_SHAPE ( 'NONE', 'NONE',  #4803 ) ;
#4556=ORIENTED_EDGE ( 'NONE', *, *, #3750, .F. ) ;
#4572=ORIENTED_EDGE ( 'NONE', *, *, #4220, .F. ) ;
#4579=CARTESIAN_POINT ( 'NONE',  ( 0.5000000000000000000, -0.2500000000000000000, 1.911797424705720116 ) ) ;
#4582=DIRECTION ( 'NONE',  ( 0.000000000000000000, 5.421010862427519705E-17, -1.000000000000000000 ) ) ;
#4585=AXIS2_PLACEMENT_3D ( 'NONE', #4678, #1417, #2389 ) ;
#4588=ADVANCED_FACE ( 'NONE', ( #2971 ), #210, .T. ) ;
#4612=FACE_BOUND ( 'NONE', #3176, .T. ) ;
#4613=CARTESIAN_POINT ( 'NONE',  ( -9.262305278225771052E-15, -0.2499999999999999445, 1.454152683131084256 ) ) ;
#4648=ORIENTED_EDGE ( 'NONE', *, *, #2384, .F. ) ;
#4660=STYLED_ITEM('',(#6027),#216);
#4671=ORIENTED_EDGE ( 'NONE', *, *, #4214, .T. ) ;
#4673=PRESENTATION_STYLE_ASSIGNMENT (( #1504 ) ) ;
#4678=CARTESIAN_POINT ( 'NONE',  ( 9.300000000000002487, 0.000000000000000000, 0.000000000000000000 ) ) ;
#4679=VECTOR ( 'NONE', #4515, 1000.000000000000000 ) ;
#4687=CYLINDRICAL_SURFACE ( 'NONE', #1611, 1.000000000000000000 ) ;
#4718=DIRECTION ( 'NONE',  ( 0.000000000000000000, 0.000000000000000000, 1.000000000000000000 ) ) ;
#4734=ORIENTED_EDGE ( 'NONE', *, *, #5517, .F. ) ;
#4736=PLANE ( 'NONE',  #5735 ) ;
#4791=PLANE ( 'NONE',  #789 ) ;
#4801=ADVANCED_FACE ( 'NONE', ( #1299 ), #2692, .F. ) ;
#4803=PRODUCT_DEFINITION ( 'UNKNOWN', '', #5744, #1693 ) ;
#4819=DIRECTION ( 'NONE',  ( 0.000000000000000000, 0.000000000000000000, 1.000000000000000000 ) ) ;
#4824=VERTEX_POINT ( 'NONE', #781 ) ;
#4831=DIRECTION ( 'NONE',  ( 0.000000000000000000, 0.000000000000000000, 1.000000000000000000 ) ) ;
#4837=CIRCLE ( 'NONE', #1919, 1.336466033005844434 ) ;
#4892=CARTESIAN_POINT ( 'NONE',  ( 0.5000000000000000000, 0.2499999999999982792, -1.911797424705720339 ) ) ;
#4896=CONICAL_SURFACE ( 'NONE', #3624, 1.886264737416298409, 0.08726646259971679309 ) ;
#4962=EDGE_LOOP ( 'NONE', ( #4324, #2711, #4424, #1529 ) ) ;
#4969=VECTOR ( 'NONE', #5370, 1000.000000000000000 ) ;
#4994=DIRECTION ( 'NONE',  ( 1.000000000000000000, 0.000000000000000000, 0.000000000000000000 ) ) ;
#5003=ORIENTED_EDGE ( 'NONE', *, *, #1900, .F. ) ;
#5009=CARTESIAN_POINT ( 'NONE',  ( 1.299999999999999156, 0.000000000000000000, 0.000000000000000000 ) ) ;
#5016=SHAPE_REPRESENTATION ( 'slotted pan head screw_iso_ISO 1580 - M2 x 8 - 8N', ( #5080 ), #4395 ) ;
#5039=DIRECTION ( 'NONE',  ( -1.000000000000000000, -0.000000000000000000, -0.000000000000000000 ) ) ;
#5042=CARTESIAN_POINT ( 'NONE',  ( 0.000000000000000000, 2.310008073021392480E-16, 1.886264737416298409 ) ) ;
#5056=ORIENTED_EDGE ( 'NONE', *, *, #5318, .T. ) ;
#5080=AXIS2_PLACEMENT_3D ( 'NONE', #3527, #4831, #667 ) ;
#5108=CIRCLE ( 'NONE', #1511, 0.5999999999999999778 ) ;
#5123=DIRECTION ( 'NONE',  ( -0.000000000000000000, 0.000000000000000000, 1.000000000000000000 ) ) ;
#5155=FACE_OUTER_BOUND ( 'NONE', #5684, .T. ) ;
#5193=ORIENTED_EDGE ( 'NONE', *, *, #26, .T. ) ;
#5194=DIRECTION ( 'NONE',  ( 0.000000000000000000, 0.000000000000000000, 1.000000000000000000 ) ) ;
#5217=FACE_OUTER_BOUND ( 'NONE', #717, .T. ) ;
#5226=DIRECTION ( 'NONE',  ( 0.000000000000000000, 0.000000000000000000, 1.000000000000000000 ) ) ;
#5240=DIRECTION ( 'NONE',  ( 0.000000000000000000, -3.552713678800500929E-15, 1.000000000000000000 ) ) ;
#5272=MECHANICAL_DESIGN_GEOMETRIC_PRESENTATION_REPRESENTATION('',(#1386),#1779);
#5300=PLANE ( 'NONE',  #5430 ) ;
#5318=EDGE_CURVE ( 'NONE', #1962, #708, #4080, .T. ) ;
#5334=EDGE_CURVE ( 'NONE', #4296, #4142, #3773, .T. ) ;
#5339=CARTESIAN_POINT ( 'NONE',  ( 0.5000000000000000000, 0.000000000000000000, 0.000000000000000000 ) ) ;
#5353=CONICAL_SURFACE ( 'NONE', #2739, 1.886264737416298409, 0.08726646259971679309 ) ;
#5370=DIRECTION ( 'NONE',  ( 0.9961946980917455452, 1.067350013832301058E-17, 0.08715574274765848506 ) ) ;
#5395=CARTESIAN_POINT ( 'NONE',  ( 0.000000000000000000, -0.2499999999999999445, 1.312875263449798879 ) ) ;
#5400=EDGE_CURVE ( 'NONE', #708, #5408, #4004, .T. ) ;
#5408=VERTEX_POINT ( 'NONE', #4892 ) ;
#5414=CARTESIAN_POINT ( 'NONE',  ( 0.000000000000000000, -0.2499999999999998335, -1.312875263449798879 ) ) ;
#5421=ORIENTED_EDGE ( 'NONE', *, *, #130, .T. ) ;
#5430=AXIS2_PLACEMENT_3D ( 'NONE', #2586, #5747, #5778 ) ;
#5436=ADVANCED_BREP_SHAPE_REPRESENTATION ( '', ( #216, #5080 ), #4395 ) ;
#5476=LINE ( 'NONE', #1774, #2628 ) ;
#5502=CARTESIAN_POINT ( 'NONE',  ( 0.5000000000000000000, -0.2500000000000000000, 1.911797424705720116 ) ) ;
#5517=EDGE_CURVE ( 'NONE', #4296, #2063, #4190, .T. ) ;
#5520=VERTEX_POINT ( 'NONE', #2569 ) ;
#5530=ORIENTED_EDGE ( 'NONE', *, *, #755, .T. ) ;
#5533=AXIS2_PLACEMENT_3D ( 'NONE', #3908, #5724, #153 ) ;
#5547=AXIS2_PLACEMENT_3D ( 'NONE', #757, #3405, #1910 ) ;
#5552=EDGE_CURVE ( 'NONE', #2883, #1725, #2177, .T. ) ;
#5579=DIRECTION ( 'NONE',  ( 0.000000000000000000, -0.000000000000000000, 1.000000000000000000 ) ) ;
#5596=DIRECTION ( 'NONE',  ( 0.000000000000000000, -1.224646799147352961E-16, 1.000000000000000000 ) ) ;
#5616=CARTESIAN_POINT ( 'NONE',  ( 0.5477065543514070267, 0.000000000000000000, 0.000000000000000000 ) ) ;
#5628=LINE ( 'NONE', #1475, #4135 ) ;
#5629=APPLICATION_CONTEXT ( 'automotive_design' ) ;
#5634=ORIENTED_EDGE ( 'NONE', *, *, #3505, .T. ) ;
#5677=ORIENTED_EDGE ( 'NONE', *, *, #3978, .T. ) ;
#5680=AXIS2_PLACEMENT_3D ( 'NONE', #2137, #4426, #4819 ) ;
#5684=EDGE_LOOP ( 'NONE', ( #3426, #2559 ) ) ;
#5691=FACE_OUTER_BOUND ( 'NONE', #5696, .T. ) ;
#5696=EDGE_LOOP ( 'NONE', ( #274, #240 ) ) ;
#5700=CARTESIAN_POINT ( 'NONE',  ( 0.000000000000000000, 0.000000000000000000, 0.000000000000000000 ) ) ;
#5724=DIRECTION ( 'NONE',  ( -1.000000000000000000, -0.000000000000000000, -0.000000000000000000 ) ) ;
#5735=AXIS2_PLACEMENT_3D ( 'NONE', #3731, #4224, #5579 ) ;
#5744=PRODUCT_DEFINITION_FORMATION_WITH_SPECIFIED_SOURCE ( 'ANY', '', #1635, .NOT_KNOWN. ) ;
#5747=DIRECTION ( 'NONE',  ( 1.000000000000000000, 0.000000000000000000, 0.000000000000000000 ) ) ;
#5760=ORIENTED_EDGE ( 'NONE', *, *, #4434, .T. ) ;
#5778=DIRECTION ( 'NONE',  ( 0.000000000000000000, 0.000000000000000000, -1.000000000000000000 ) ) ;
#5794=ADVANCED_FACE ( 'NONE', ( #5155 ), #2722, .T. ) ;
#5804=DIRECTION ( 'NONE',  ( -0.000000000000000000, 0.000000000000000000, 1.000000000000000000 ) ) ;
#5808=CARTESIAN_POINT ( 'NONE',  ( 0.000000000000000000, 0.2499999999999982792, 2.000000000000001776 ) ) ;
#5830=TOROIDAL_SURFACE ( 'NONE', #1671, 1.336466033005844434, 0.5999999999999999778 ) ;
#5839=ADVANCED_FACE ( 'NONE', ( #4316 ), #5830, .T. ) ;
#5866=ADVANCED_FACE ( 'NONE', ( #5217 ), #5353, .T. ) ;
#5873=UNCERTAINTY_MEASURE_WITH_UNIT (LENGTH_MEASURE( 1.000000000000000082E-05 ), #2695, 'distance_accuracy_value', 'NONE');
#5905=VECTOR ( 'NONE', #4147, 1000.000000000000000 ) ;
#5942=( NAMED_UNIT ( * ) SI_UNIT ( $, .STERADIAN. ) SOLID_ANGLE_UNIT ( ) );
#6021=COLOUR_RGB('Black',0.12,0.14,0.17);
#6022=FILL_AREA_STYLE_COLOUR('',#6021);
#6023=FILL_AREA_STYLE('',(#6022));
#6024=SURFACE_STYLE_FILL_AREA(#6023);
#6025=SURFACE_SIDE_STYLE('',(#6024));
#6026=SURFACE_STYLE_USAGE(.BOTH.,#6025);
#6027=PRESENTATION_STYLE_ASSIGNMENT((#6026));
ENDSEC;
END-ISO-10303-21;
